ISO-10303-21;
HEADER;
FILE_DESCRIPTION (('STEP AP214'),
    '1' );
FILE_NAME ('hex nut style 1_am_B18.2.4.1M - Hex nut, Style 1,  M10 x 1.5, with 16mm WAF --D-N.step',
    '2026-10-24T15:53:57',
    ( '' ),
    ( '' ),
    'SwSTEP 2.0',
    'SolidWorks 2025',
    '' );
FILE_SCHEMA (( 'AUTOMOTIVE_DESIGN' ));
ENDSEC;

DATA;
#14=DIRECTION ( 'NONE',  ( 0.000000000000000000, 0.000000000000000000, 1.000000000000000000 ) ) ;
#30=CIRCLE ( 'NONE', #2975, 8.000000000000007105 ) ;
#84=DIRECTION ( 'NONE',  ( 0.000000000000000000, 0.000000000000000000, 1.000000000000000000 ) ) ;
#87=EDGE_CURVE ( 'NONE', #4142, #6381, #1356, .T. ) ;
#92=VERTEX_POINT ( 'NONE', #1262 ) ;
#96=DIRECTION ( 'NONE',  ( 0.000000000000000000, 0.000000000000000000, 1.000000000000000000 ) ) ;
#97=CARTESIAN_POINT ( 'NONE',  ( 8.000000000000127898, -3.098204225878314233, -0.3157906771919719024 ) ) ;
#100=ORIENTED_EDGE ( 'NONE', *, *, #87, .T. ) ;
#123=AXIS2_PLACEMENT_3D ( 'NONE', #533, #8501, #5709 ) ;
#129=AXIS2_PLACEMENT_3D ( 'NONE', #5257, #6018, #4697 ) ;
#133=EDGE_CURVE ( 'NONE', #2369, #4500, #873, .T. ) ;
#154=ADVANCED_FACE ( 'NONE', ( #2295 ), #1559, .T. ) ;
#168=AXIS2_PLACEMENT_3D ( 'NONE', #382, #5715, #8345 ) ;
#174=VECTOR ( 'NONE', #663, 1000.000000000000000 ) ;
#176=AXIS2_PLACEMENT_3D ( 'NONE', #7035, #983, #7228 ) ;
#193=CARTESIAN_POINT ( 'NONE',  ( 8.000000000000229150, -1.665334536937734811E-13, 0.000000000000000000 ) ) ;
#212=ADVANCED_BREP_SHAPE_REPRESENTATION ( '', ( #5685, #7563 ), #1720 ) ;
#243=CARTESIAN_POINT ( 'NONE',  ( 0.000000000000000000, 0.000000000000000000, -8.400000000000018119 ) ) ;
#268=CONICAL_SURFACE ( 'NONE', #8331, 8.000000000000007105, 1.047197551196597631 ) ;
#288=DIRECTION ( 'NONE',  ( 0.000000000000000000, 0.000000000000000000, 1.000000000000000000 ) ) ;
#314=CARTESIAN_POINT ( 'NONE',  ( -8.000000000000001776, 0.7809653281576423023, -8.400000000000011013 ) ) ;
#331=AXIS2_PLACEMENT_3D ( 'NONE', #1287, #6747, #4081 ) ;
#335=EDGE_CURVE ( 'NONE', #2009, #7164, #7911, .T. ) ;
#342=DIRECTION ( 'NONE',  ( -1.000000000000000000, -8.881784197001244435E-16, 0.000000000000000000 ) ) ;
#353=ORIENTED_EDGE ( 'NONE', *, *, #7620, .T. ) ;
#361=CARTESIAN_POINT ( 'NONE',  ( 1.110223024625156540E-13, 9.237604307033992157, -8.400000000000018119 ) ) ;
#363=VERTEX_POINT ( 'NONE', #3075 ) ;
#371=CARTESIAN_POINT ( 'NONE',  ( 0.000000000000000000, 0.000000000000000000, -8.400000000000018119 ) ) ;
#373=ORIENTED_EDGE ( 'NONE', *, *, #1689, .F. ) ;
#375=CARTESIAN_POINT ( 'NONE',  ( 8.000000000000229150, -1.665334536937734811E-13, -8.400000000000018119 ) ) ;
#382=CARTESIAN_POINT ( 'NONE',  ( 0.000000000000000000, 0.000000000000000000, -8.400000000000018119 ) ) ;
#385=CARTESIAN_POINT ( 'NONE',  ( 0.000000000000000000, 0.000000000000000000, -8.401000000000047763 ) ) ;
#390=ORIENTED_EDGE ( 'NONE', *, *, #2485, .F. ) ;
#400=CARTESIAN_POINT ( 'NONE',  ( 4.000000000000114575, 6.928203230275597591, -8.400000000000018119 ) ) ;
#406=CARTESIAN_POINT ( 'NONE',  ( 4.000000000000114575, 6.928203230275597591, -8.400000000000018119 ) ) ;
#417=CARTESIAN_POINT ( 'NONE',  ( 8.000000000000117240, 3.871967595402003859, -7.901061386767532113 ) ) ;
#456=CARTESIAN_POINT ( 'NONE',  ( -4.681481898396970820, 6.534749472788062619, -8.400000000000073186 ) ) ;
#462=VERTEX_POINT ( 'NONE', #2562 ) ;
#465=ORIENTED_EDGE ( 'NONE', *, *, #5590, .T. ) ;
#485=EDGE_CURVE ( 'NONE', #7120, #4330, #2916, .T. ) ;
#487=CARTESIAN_POINT ( 'NONE',  ( -8.000000000000007105, 1.110223024625156540E-13, 0.000000000000000000 ) ) ;
#494=EDGE_CURVE ( 'NONE', #3910, #4142, #3557, .T. ) ;
#502=ORIENTED_EDGE ( 'NONE', *, *, #6495, .T. ) ;
#504=ORIENTED_EDGE ( 'NONE', *, *, #3487, .F. ) ;
#533=CARTESIAN_POINT ( 'NONE',  ( -8.000000000000007105, 4.618802153517009401, -8.400000000000018119 ) ) ;
#535=EDGE_CURVE ( 'NONE', #6830, #5405, #2458, .T. ) ;
#556=CARTESIAN_POINT ( 'NONE',  ( 8.000000000000229150, -1.665334536937734811E-13, -8.400000000000018119 ) ) ;
#557=ORIENTED_EDGE ( 'NONE', *, *, #5105, .F. ) ;
#567=CARTESIAN_POINT ( 'NONE',  ( -8.000000000000007105, -4.618802153517065356, -0.7145311798163467287 ) ) ;
#583=ORIENTED_EDGE ( 'NONE', *, *, #3619, .F. ) ;
#584=CARTESIAN_POINT ( 'NONE',  ( -8.000000000000007105, -4.618802153517065356, -0.7145311798163467287 ) ) ;
#587=LINE ( 'NONE', #3243, #4960 ) ;
#628=CARTESIAN_POINT ( 'NONE',  ( 0.000000000000000000, 0.000000000000000000, 0.000000000000000000 ) ) ;
#638=ORIENTED_EDGE ( 'NONE', *, *, #7578, .F. ) ;
#645=CARTESIAN_POINT ( 'NONE',  ( -4.000000000000003553, 6.928203230275431501, 0.000000000000000000 ) ) ;
#663=DIRECTION ( 'NONE',  ( 0.000000000000000000, 0.000000000000000000, 1.000000000000000000 ) ) ;
#678=LINE ( 'NONE', #5249, #6920 ) ;
#754=DIRECTION ( 'NONE',  ( 1.000000000000000000, 8.881784197001244435E-16, 0.000000000000000000 ) ) ;
#755=EDGE_LOOP ( 'NONE', ( #1822, #2108, #4913 ) ) ;
#759=ADVANCED_FACE ( 'NONE', ( #6786 ), #4895, .F. ) ;
#760=DIRECTION ( 'NONE',  ( -0.000000000000000000, -0.000000000000000000, 1.000000000000000000 ) ) ;
#761=ORIENTED_EDGE ( 'NONE', *, *, #8539, .T. ) ;
#764=CARTESIAN_POINT ( 'NONE',  ( 0.000000000000000000, 0.000000000000000000, -8.401000000000047763 ) ) ;
#770=DIRECTION ( 'NONE',  ( 0.000000000000000000, 0.000000000000000000, -1.000000000000000000 ) ) ;
#771=CARTESIAN_POINT ( 'NONE',  ( -1.313474075707264488, -8.479269695850916833, -8.083279549040147671 ) ) ;
#772=ORIENTED_EDGE ( 'NONE', *, *, #8153, .F. ) ;
#781=DIRECTION ( 'NONE',  ( -1.000000000000000000, -8.881784197001244435E-16, 0.000000000000000000 ) ) ;
#784=CARTESIAN_POINT ( 'NONE',  ( -8.000000000000007105, 4.618802153517009401, -8.400000000000018119 ) ) ;
#797=CIRCLE ( 'NONE', #4688, 5.500000000000024869 ) ;
#806=CARTESIAN_POINT ( 'NONE',  ( -8.000000000000003553, -0.7805016046290118581, 5.039846036163083862E-15 ) ) ;
#809=DIRECTION ( 'NONE',  ( -0.9237280213470678847, -0.3830490080632384942, 0.000000000000000000 ) ) ;
#817=EDGE_LOOP ( 'NONE', ( #4283, #4249, #761, #638, #772, #5815 ) ) ;
#847=ORIENTED_EDGE ( 'NONE', *, *, #1734, .T. ) ;
#873=CIRCLE ( 'NONE', #3915, 5.500000000000024869 ) ;
#874=DIRECTION ( 'NONE',  ( -1.000000000000000000, -8.881784197001244435E-16, 0.000000000000000000 ) ) ;
#890=B_SPLINE_CURVE_WITH_KNOTS ( 'NONE', 3,
 ( #4953, #8139, #7488, #2212, #8228, #5582 ),
 .UNSPECIFIED., .F., .F.,
 ( 4, 2, 4 ),
 ( 2.380731629387024750E-07, 0.002336973833157600638, 0.004673709593152262400 ),
 .UNSPECIFIED. ) ;
#904=CARTESIAN_POINT ( 'NONE',  ( 0.000000000000000000, 0.000000000000000000, -8.400000000000018119 ) ) ;
#908=CARTESIAN_POINT ( 'NONE',  ( -6.689127551062048482, -5.375634714784658819, -8.082649155111331751 ) ) ;
#917=CARTESIAN_POINT ( 'NONE',  ( -8.000000000000007105, 3.871967595402132645, -0.4989386132324617473 ) ) ;
#920=ORIENTED_EDGE ( 'NONE', *, *, #3291, .T. ) ;
#930=EDGE_CURVE ( 'NONE', #462, #4330, #30, .T. ) ;
#983=DIRECTION ( 'NONE',  ( 0.000000000000000000, 0.000000000000000000, 1.000000000000000000 ) ) ;
#1035=B_SPLINE_CURVE_WITH_KNOTS ( 'NONE', 3,
 ( #4450, #8453, #2403, #2314, #7756, #2444, #6943, #2484 ),
 .UNSPECIFIED., .F., .F.,
 ( 4, 2, 2, 4 ),
 ( 0.004673709593152262400, 0.005837709341827771771, 0.007001709090503281142, 0.009329708587854299018 ),
 .UNSPECIFIED. ) ;
#1051=CARTESIAN_POINT ( 'NONE',  ( 0.000000000000000000, 0.000000000000000000, -8.400000000000018119 ) ) ;
#1078=PLANE ( 'NONE',  #3345 ) ;
#1099=CARTESIAN_POINT ( 'NONE',  ( -5.354491962338076227, 6.146186931204334236, -8.331901280394644616 ) ) ;
#1100=EDGE_CURVE ( 'NONE', #6142, #92, #6057, .T. ) ;
#1111=CLOSED_SHELL ( 'NONE', ( #1558, #3745, #5880, #1315, #2465, #1923, #2389, #8392, #4690, #2185, #2012, #7267, #3909, #5796, #8296, #154, #7284, #6547, #2936, #1396, #8597, #759 ) ) ;
#1133=FACE_BOUND ( 'NONE', #2656, .T. ) ;
#1155=FACE_OUTER_BOUND ( 'NONE', #817, .T. ) ;
#1185=CARTESIAN_POINT ( 'NONE',  ( 8.000000000000117240, 4.618802153516954334, -8.400000000000018119 ) ) ;
#1223=VERTEX_POINT ( 'NONE', #5770 ) ;
#1230=CARTESIAN_POINT ( 'NONE',  ( -5.690023276062465385, -5.952467836904175691, -0.1306530452038474899 ) ) ;
#1235=CIRCLE ( 'NONE', #129, 5.500000000000024869 ) ;
#1237=CARTESIAN_POINT ( 'NONE',  ( 0.000000000000000000, 0.000000000000000000, -8.400000000000018119 ) ) ;
#1247=CONICAL_SURFACE ( 'NONE', #6948, 8.000000000000007105, 1.047197551196597631 ) ;
#1257=CARTESIAN_POINT ( 'NONE',  ( -4.000000000000003553, 6.928203230275431501, -8.400000000000018119 ) ) ;
#1262=CARTESIAN_POINT ( 'NONE',  ( -8.000000000000007105, 1.110223024625156540E-13, -8.400000000000018119 ) ) ;
#1269=CARTESIAN_POINT ( 'NONE',  ( -5.080504117408896292, -2.106769544347821377, 0.000000000000000000 ) ) ;
#1282=CARTESIAN_POINT ( 'NONE',  ( -4.339467034331305761, -6.732211846623399332, -3.359396196281597955E-14 ) ) ;
#1287=CARTESIAN_POINT ( 'NONE',  ( 0.000000000000000000, 0.000000000000000000, 0.000000000000000000 ) ) ;
#1294=EDGE_CURVE ( 'NONE', #7390, #3622, #2823, .T. ) ;
#1298=CARTESIAN_POINT ( 'NONE',  ( -7.345652830558729640, 4.996589667937282542, -0.4964154566687483117 ) ) ;
#1303=DIRECTION ( 'NONE',  ( 0.000000000000000000, 0.000000000000000000, -1.000000000000000000 ) ) ;
#1315=ADVANCED_FACE ( 'NONE', ( #7307 ), #1341, .F. ) ;
#1324=ORIENTED_EDGE ( 'NONE', *, *, #1689, .T. ) ;
#1333=B_SPLINE_CURVE_WITH_KNOTS ( 'NONE', 3,
 ( #5660, #1749, #7071, #1099, #456, #1257 ),
 .UNSPECIFIED., .F., .F.,
 ( 4, 2, 4 ),
 ( 2.380731629664482303E-07, 0.002336973833157514335, 0.004673709593152062039 ),
 .UNSPECIFIED. ) ;
#1341=PLANE ( 'NONE',  #7859 ) ;
#1355=CARTESIAN_POINT ( 'NONE',  ( 3.319543390096077129, -7.321065037175521262, -0.01688885742782669439 ) ) ;
#1356=LINE ( 'NONE', #7193, #8234 ) ;
#1378=ORIENTED_EDGE ( 'NONE', *, *, #8008, .F. ) ;
#1381=EDGE_CURVE ( 'NONE', #8461, #6830, #3663, .T. ) ;
#1383=CARTESIAN_POINT ( 'NONE',  ( -5.690023276062465385, -5.952467836904175691, -8.269346954796169769 ) ) ;
#1389=CONICAL_SURFACE ( 'NONE', #3050, 8.000000000000007105, 1.047197551196597631 ) ;
#1396=ADVANCED_FACE ( 'NONE', ( #6880 ), #7177, .T. ) ;
#1417=CARTESIAN_POINT ( 'NONE',  ( -8.000000000000000000, -3.867591403079189583, -0.4976753153245850880 ) ) ;
#1424=CARTESIAN_POINT ( 'NONE',  ( 0.000000000000000000, 0.000000000000000000, 0.000000000000000000 ) ) ;
#1444=CARTESIAN_POINT ( 'NONE',  ( 2.309976723937650078, -7.903938623646967088, -0.1306530452038709711 ) ) ;
#1450=DIRECTION ( 'NONE',  ( 0.000000000000000000, 0.000000000000000000, -1.000000000000000000 ) ) ;
#1451=ORIENTED_EDGE ( 'NONE', *, *, #3541, .F. ) ;
#1458=DIRECTION ( 'NONE',  ( -1.000000000000000000, -8.881784197001244435E-16, 0.000000000000000000 ) ) ;
#1462=CARTESIAN_POINT ( 'NONE',  ( 0.000000000000000000, 0.000000000000000000, -8.400000000000018119 ) ) ;
#1473=DIRECTION ( 'NONE',  ( -1.000000000000000000, -8.881784197001244435E-16, 0.000000000000000000 ) ) ;
#1499=DIRECTION ( 'NONE',  ( -0.5000000000000033307, -0.8660254037844367092, 0.000000000000000000 ) ) ;
#1502=CARTESIAN_POINT ( 'NONE',  ( 0.000000000000000000, -9.237604307034075646, -7.685468820183672278 ) ) ;
#1513=DIRECTION ( 'NONE',  ( 1.000000000000000000, 8.881784197001244435E-16, 0.000000000000000000 ) ) ;
#1531=CARTESIAN_POINT ( 'NONE',  ( -1.310872448937907997, 8.480771745766357839, -8.082649155111395700 ) ) ;
#1547=ORIENTED_EDGE ( 'NONE', *, *, #5549, .T. ) ;
#1558=ADVANCED_FACE ( 'NONE', ( #7044 ), #3696, .F. ) ;
#1559=CONICAL_SURFACE ( 'NONE', #8242, 8.000000000000007105, 1.047197551196597631 ) ;
#1560=CARTESIAN_POINT ( 'NONE',  ( -8.000000000000005329, 1.572549600175648044, -0.06894455525513798477 ) ) ;
#1577=CARTESIAN_POINT ( 'NONE',  ( -8.000000000000007105, 3.871967595402025175, -7.901061386767586292 ) ) ;
#1590=ORIENTED_EDGE ( 'NONE', *, *, #2485, .T. ) ;
#1602=ORIENTED_EDGE ( 'NONE', *, *, #4265, .F. ) ;
#1615=CARTESIAN_POINT ( 'NONE',  ( 1.110223024625156540E-13, -9.237604307034075646, -8.400000000000018119 ) ) ;
#1619=ORIENTED_EDGE ( 'NONE', *, *, #6904, .F. ) ;
#1621=CARTESIAN_POINT ( 'NONE',  ( -7.999999999999896083, -4.618802153517121312, -8.400000000000018119 ) ) ;
#1627=VERTEX_POINT ( 'NONE', #5759 ) ;
#1632=CARTESIAN_POINT ( 'NONE',  ( 0.000000000000000000, 0.000000000000000000, 0.000000000000000000 ) ) ;
#1635=DIRECTION ( 'NONE',  ( 0.000000000000000000, 0.000000000000000000, -1.000000000000000000 ) ) ;
#1682=DIRECTION ( 'NONE',  ( 0.000000000000000000, 0.000000000000000000, -1.000000000000000000 ) ) ;
#1689=EDGE_CURVE ( 'NONE', #4831, #4500, #587, .T. ) ;
#1708=CARTESIAN_POINT ( 'NONE',  ( 8.000000000000007105, 4.618802153516899267, -7.685468820183672278 ) ) ;
#1714=EDGE_CURVE ( 'NONE', #4831, #6936, #797, .T. ) ;
#1720=( GEOMETRIC_REPRESENTATION_CONTEXT ( 3 ) GLOBAL_UNCERTAINTY_ASSIGNED_CONTEXT ( ( #1737 ) ) GLOBAL_UNIT_ASSIGNED_CONTEXT ( ( #5710, #8383, #7076 ) ) REPRESENTATION_CONTEXT ( 'NONE', 'WORKASPACE' ) );
#1724=CARTESIAN_POINT ( 'NONE',  ( 8.000000000000007105, -4.618802153517121312, -7.685468820183672278 ) ) ;
#1731=EDGE_LOOP ( 'NONE', ( #7583, #7141, #2198, #8600, #6128, #1922 ) ) ;
#1734=EDGE_CURVE ( 'NONE', #6936, #2369, #678, .T. ) ;
#1736=CIRCLE ( 'NONE', #4957, 8.000000000000007105 ) ;
#1737=UNCERTAINTY_MEASURE_WITH_UNIT (LENGTH_MEASURE( 1.000000000000000082E-05 ), #5710, 'distance_accuracy_value', 'NONE');
#1744=CARTESIAN_POINT ( 'NONE',  ( 5.690023276062453839, 5.952467836904148157, -8.269346954796187532 ) ) ;
#1749=CARTESIAN_POINT ( 'NONE',  ( -7.345652830558644375, 4.996589667937334056, -7.903584543331295009 ) ) ;
#1750=DIRECTION ( 'NONE',  ( 1.000000000000000000, 8.881784197001244435E-16, 0.000000000000000000 ) ) ;
#1764=CARTESIAN_POINT ( 'NONE',  ( 1.110223024625156540E-13, 9.237604307033992157, -7.685468820183672278 ) ) ;
#1765=CARTESIAN_POINT ( 'NONE',  ( 4.000000000000114575, 6.928203230275597591, 0.000000000000000000 ) ) ;
#1776=ORIENTED_EDGE ( 'NONE', *, *, #1381, .F. ) ;
#1822=ORIENTED_EDGE ( 'NONE', *, *, #3541, .T. ) ;
#1871=ORIENTED_EDGE ( 'NONE', *, *, #8153, .T. ) ;
#1922=ORIENTED_EDGE ( 'NONE', *, *, #5590, .F. ) ;
#1923=ADVANCED_FACE ( 'NONE', ( #4853 ), #2284, .T. ) ;
#1926=EDGE_CURVE ( 'NONE', #92, #3910, #3735, .T. ) ;
#1946=EDGE_LOOP ( 'NONE', ( #100, #2888, #6161, #6293, #390, #5727 ) ) ;
#1955=AXIS2_PLACEMENT_3D ( 'NONE', #3957, #5976, #8006 ) ;
#1956=ORIENTED_EDGE ( 'NONE', *, *, #930, .T. ) ;
#1970=EDGE_LOOP ( 'NONE', ( #4625, #583, #3432, #353, #6761, #8091 ) ) ;
#1980=AXIS2_PLACEMENT_3D ( 'NONE', #7324, #4010, #6037 ) ;
#1981=DIRECTION ( 'NONE',  ( 0.000000000000000000, 0.000000000000000000, 1.000000000000000000 ) ) ;
#2002=AXIS2_PLACEMENT_3D ( 'NONE', #3465, #6737, #2763 ) ;
#2006=CARTESIAN_POINT ( 'NONE',  ( 8.000000000000122569, 0.7809653281574673311, -6.100924209188546528E-14 ) ) ;
#2009=VERTEX_POINT ( 'NONE', #3147 ) ;
#2012=ADVANCED_FACE ( 'NONE', ( #5099 ), #268, .T. ) ;
#2025=DIRECTION ( 'NONE',  ( -0.000000000000000000, -0.000000000000000000, 1.000000000000000000 ) ) ;
#2030=CARTESIAN_POINT ( 'NONE',  ( 5.355005115540955707, 6.145890662064651622, -0.08224679563973515128 ) ) ;
#2035=B_SPLINE_CURVE_WITH_KNOTS ( 'NONE', 3,
 ( #7321, #5410, #1355, #4799, #1444, #6672, #4054, #8062 ),
 .UNSPECIFIED., .F., .F.,
 ( 4, 2, 2, 4 ),
 ( 0.004673709593152262400, 0.005837709341827771771, 0.007001709090503281142, 0.009329708587854299018 ),
 .UNSPECIFIED. ) ;
#2044=B_SPLINE_CURVE_WITH_KNOTS ( 'NONE', 3,
 ( #1502, #5566, #771, #8216, #3427, #5437 ),
 .UNSPECIFIED., .F., .F.,
 ( 4, 2, 4 ),
 ( 2.380731630569847498E-07, 0.002336973833157701252, 0.004673709593152344799 ),
 .UNSPECIFIED. ) ;
#2045=LINE ( 'NONE', #784, #5137 ) ;
#2084=CARTESIAN_POINT ( 'NONE',  ( -1.313474075707264488, -8.479269695850916833, -0.3167204509598732787 ) ) ;
#2108=ORIENTED_EDGE ( 'NONE', *, *, #3505, .F. ) ;
#2130=CARTESIAN_POINT ( 'NONE',  ( 4.339467034331248918, 6.732211846623394891, -1.598414698939908181E-14 ) ) ;
#2150=ORIENTED_EDGE ( 'NONE', *, *, #4088, .T. ) ;
#2185=ADVANCED_FACE ( 'NONE', ( #3881 ), #1247, .T. ) ;
#2192=VERTEX_POINT ( 'NONE', #8117 ) ;
#2195=CARTESIAN_POINT ( 'NONE',  ( -2.644994884459048290, 7.710515798486305528, -8.317753204360352370 ) ) ;
#2196=CARTESIAN_POINT ( 'NONE',  ( -8.000000000000007105, 1.110223024625156540E-13, -8.400000000000018119 ) ) ;
#2198=ORIENTED_EDGE ( 'NONE', *, *, #3984, .T. ) ;
#2200=EDGE_LOOP ( 'NONE', ( #2301, #8458, #3544 ) ) ;
#2209=CARTESIAN_POINT ( 'NONE',  ( -7.347286611336995676, -4.995646404165323240, -7.903039949738239756 ) ) ;
#2210=CARTESIAN_POINT ( 'NONE',  ( 8.000000000000229150, -1.665334536937734811E-13, -8.400000000000018119 ) ) ;
#2212=CARTESIAN_POINT ( 'NONE',  ( 5.354491962338145505, -6.146186931204510984, -8.331901280394534481 ) ) ;
#2217=EDGE_CURVE ( 'NONE', #6543, #462, #3178, .T. ) ;
#2284=PLANE ( 'NONE',  #6650 ) ;
#2295=FACE_OUTER_BOUND ( 'NONE', #755, .T. ) ;
#2298=ORIENTED_EDGE ( 'NONE', *, *, #6981, .T. ) ;
#2301=ORIENTED_EDGE ( 'NONE', *, *, #494, .T. ) ;
#2314=CARTESIAN_POINT ( 'NONE',  ( 2.644994884459147766, -7.710515798486462735, -8.317753204360245789 ) ) ;
#2323=ORIENTED_EDGE ( 'NONE', *, *, #7306, .F. ) ;
#2339=EDGE_CURVE ( 'NONE', #5854, #2009, #6338, .T. ) ;
#2346=UNCERTAINTY_MEASURE_WITH_UNIT (LENGTH_MEASURE( 1.000000000000000082E-05 ), #5167, 'distance_accuracy_value', 'NONE');
#2369=VERTEX_POINT ( 'NONE', #3635 ) ;
#2389=ADVANCED_FACE ( 'NONE', ( #4498 ), #6500, .T. ) ;
#2403=CARTESIAN_POINT ( 'NONE',  ( 3.319543390096077129, -7.321065037175521262, -8.383111142572191810 ) ) ;
#2428=CARTESIAN_POINT ( 'NONE',  ( 0.000000000000000000, 0.000000000000000000, 0.000000000000000000 ) ) ;
#2441=DIRECTION ( 'NONE',  ( 0.000000000000000000, 0.000000000000000000, 1.000000000000000000 ) ) ;
#2444=CARTESIAN_POINT ( 'NONE',  ( 1.310872448938031010, -8.480771745766503500, -8.082649155111303330 ) ) ;
#2454=EDGE_LOOP ( 'NONE', ( #3882, #6076, #7466 ) ) ;
#2458=CIRCLE ( 'NONE', #6798, 8.000000000000007105 ) ;
#2465=ADVANCED_FACE ( 'NONE', ( #7507 ), #7590, .T. ) ;
#2481=CARTESIAN_POINT ( 'NONE',  ( 0.000000000000000000, 0.000000000000000000, 0.000000000000000000 ) ) ;
#2484=CARTESIAN_POINT ( 'NONE',  ( 0.000000000000000000, -9.237604307034075646, -7.685468820183672278 ) ) ;
#2485=EDGE_CURVE ( 'NONE', #92, #1627, #6350, .T. ) ;
#2562=CARTESIAN_POINT ( 'NONE',  ( 4.000000000000003553, -6.928203230275542523, 0.000000000000000000 ) ) ;
#2566=ORIENTED_EDGE ( 'NONE', *, *, #3303, .F. ) ;
#2581=AXIS2_PLACEMENT_3D ( 'NONE', #4258, #3607, #1473 ) ;
#2595=ORIENTED_EDGE ( 'NONE', *, *, #535, .F. ) ;
#2602=CARTESIAN_POINT ( 'NONE',  ( -4.681481898396988583, 6.534749472788051960, 5.236696493104986416E-14 ) ) ;
#2635=AXIS2_PLACEMENT_3D ( 'NONE', #1424, #770, #4650 ) ;
#2649=CARTESIAN_POINT ( 'NONE',  ( -4.339467034331305761, -6.732211846623399332, -8.399999999999982592 ) ) ;
#2656=EDGE_LOOP ( 'NONE', ( #7625, #5641 ) ) ;
#2680=ORIENTED_EDGE ( 'NONE', *, *, #6981, .F. ) ;
#2683=EDGE_CURVE ( 'NONE', #1627, #7390, #2045, .T. ) ;
#2698=CARTESIAN_POINT ( 'NONE',  ( 4.000000000000003553, -6.928203230275542523, 0.000000000000000000 ) ) ;
#2714=PLANE ( 'NONE',  #1980 ) ;
#2735=CARTESIAN_POINT ( 'NONE',  ( -3.660532965668796823, 7.124194613927540054, 5.481721948921974147E-14 ) ) ;
#2736=CARTESIAN_POINT ( 'NONE',  ( 6.689127551062064470, 5.375634714784610857, -0.3173508448886774302 ) ) ;
#2741=CARTESIAN_POINT ( 'NONE',  ( -8.000000000000007105, 4.618802153517009401, -0.7145311798163467287 ) ) ;
#2752=CARTESIAN_POINT ( 'NONE',  ( -8.000000000000003553, -0.7805016046290103038, -8.400000000000023448 ) ) ;
#2760=ORIENTED_EDGE ( 'NONE', *, *, #1100, .F. ) ;
#2763=DIRECTION ( 'NONE',  ( 1.000000000000000000, 8.881784197001244435E-16, 0.000000000000000000 ) ) ;
#2811=DIRECTION ( 'NONE',  ( -1.000000000000000000, -8.881784197001244435E-16, 0.000000000000000000 ) ) ;
#2823=B_SPLINE_CURVE_WITH_KNOTS ( 'NONE', 3,
 ( #2741, #1298, #6565, #8563, #2602, #645 ),
 .UNSPECIFIED., .F., .F.,
 ( 4, 2, 4 ),
 ( 2.380731628432377855E-07, 0.002336973833157452319, 0.004673709593152062039 ),
 .UNSPECIFIED. ) ;
#2832=CARTESIAN_POINT ( 'NONE',  ( 0.000000000000000000, 0.000000000000000000, -8.400000000000018119 ) ) ;
#2836=CARTESIAN_POINT ( 'NONE',  ( -8.000000000000007105, -4.618802153517065356, -7.685468820183672278 ) ) ;
#2859=CARTESIAN_POINT ( 'NONE',  ( 0.000000000000000000, 0.000000000000000000, 0.000000000000000000 ) ) ;
#2871=CARTESIAN_POINT ( 'NONE',  ( -8.000000000000007105, 1.110223024625156540E-13, 0.000000000000000000 ) ) ;
#2888=ORIENTED_EDGE ( 'NONE', *, *, #3505, .T. ) ;
#2916=B_SPLINE_CURVE_WITH_KNOTS ( 'NONE', 3,
 ( #8046, #4612, #2084, #7260, #4743, #8410 ),
 .UNSPECIFIED., .F., .F.,
 ( 4, 2, 4 ),
 ( 2.380731630570001552E-07, 0.002336973833157701252, 0.004673709593152344799 ),
 .UNSPECIFIED. ) ;
#2918=ORIENTED_EDGE ( 'NONE', *, *, #3859, .T. ) ;
#2928=ORIENTED_EDGE ( 'NONE', *, *, #1734, .F. ) ;
#2936=ADVANCED_FACE ( 'NONE', ( #7662 ), #3342, .T. ) ;
#2944=ORIENTED_EDGE ( 'NONE', *, *, #6930, .F. ) ;
#2947=DIRECTION ( 'NONE',  ( 1.000000000000000000, 8.881784197001244435E-16, 0.000000000000000000 ) ) ;
#2957=CIRCLE ( 'NONE', #176, 5.500000000000024869 ) ;
#2975=AXIS2_PLACEMENT_3D ( 'NONE', #3618, #4959, #4311 ) ;
#2976=CARTESIAN_POINT ( 'NONE',  ( -8.000000000000005329, 1.572549600175600970, -8.331055444744887239 ) ) ;
#2992=CARTESIAN_POINT ( 'NONE',  ( 8.000000000000007105, -4.618802153517121312, -7.685468820183672278 ) ) ;
#3000=ORIENTED_EDGE ( 'NONE', *, *, #3291, .F. ) ;
#3016=ORIENTED_EDGE ( 'NONE', *, *, #930, .F. ) ;
#3022=CARTESIAN_POINT ( 'NONE',  ( 8.000000000000120792, 1.572549600175473739, -8.331055444744837502 ) ) ;
#3050=AXIS2_PLACEMENT_3D ( 'NONE', #1237, #96, #6060 ) ;
#3057=CARTESIAN_POINT ( 'NONE',  ( 4.339467034331248918, 6.732211846623395779, -8.400000000000000355 ) ) ;
#3075=CARTESIAN_POINT ( 'NONE',  ( 4.000000000000003553, -6.928203230275542523, -8.400000000000018119 ) ) ;
#3096=CARTESIAN_POINT ( 'NONE',  ( 6.689127551062064470, 5.375634714784610857, -8.082649155111342409 ) ) ;
#3108=LINE ( 'NONE', #1185, #8070 ) ;
#3133=ORIENTED_EDGE ( 'NONE', *, *, #1714, .F. ) ;
#3147=CARTESIAN_POINT ( 'NONE',  ( 1.110223024625156540E-13, 9.237604307033992157, -0.7145311798163467287 ) ) ;
#3157=CARTESIAN_POINT ( 'NONE',  ( 4.000000000000114575, 6.928203230275597591, -8.400000000000018119 ) ) ;
#3167=SHAPE_REPRESENTATION ( 'hex nut style 1_am_B18.2.4.1M - Hex nut, Style 1,  M10 x 1.5, with 16mm WAF --D-N', ( #7563 ), #1720 ) ;
#3178=CIRCLE ( 'NONE', #4297, 8.000000000000007105 ) ;
#3181=EDGE_LOOP ( 'NONE', ( #7921, #2760, #2323, #2595, #504, #3000 ) ) ;
#3211=( NAMED_UNIT ( * ) SI_UNIT ( $, .STERADIAN. ) SOLID_ANGLE_UNIT ( ) );
#3243=CARTESIAN_POINT ( 'NONE',  ( -5.080504117408896292, -2.106769544347821377, -8.401000000000047763 ) ) ;
#3259=PRODUCT_DEFINITION_FORMATION_WITH_SPECIFIED_SOURCE ( 'ANY', '', #7853, .NOT_KNOWN. ) ;
#3291=EDGE_CURVE ( 'NONE', #3910, #363, #6042, .T. ) ;
#3298=CARTESIAN_POINT ( 'NONE',  ( 0.000000000000000000, 0.000000000000000000, 0.000000000000000000 ) ) ;
#3303=EDGE_CURVE ( 'NONE', #5371, #7390, #3422, .T. ) ;
#3342=CONICAL_SURFACE ( 'NONE', #4322, 8.000000000000007105, 1.047197551196597631 ) ;
#3345=AXIS2_PLACEMENT_3D ( 'NONE', #4343, #3815, #7011 ) ;
#3354=CARTESIAN_POINT ( 'NONE',  ( -8.000000000000000000, -3.867591403079186030, -7.902324684675432920 ) ) ;
#3378=CARTESIAN_POINT ( 'NONE',  ( 8.000000000000007105, -4.618802153517121312, -0.7145311798163467287 ) ) ;
#3394=CARTESIAN_POINT ( 'NONE',  ( 8.000000000000007105, 4.618802153516899267, -7.685468820183672278 ) ) ;
#3421=DIRECTION ( 'NONE',  ( 0.000000000000000000, 0.000000000000000000, 1.000000000000000000 ) ) ;
#3422=B_SPLINE_CURVE_WITH_KNOTS ( 'NONE', 3,
 ( #2871, #4877, #1560, #6888, #917, #4596 ),
 .UNSPECIFIED., .F., .F.,
 ( 4, 2, 4 ),
 ( 0.01291313371729486958, 0.01525081363757331207, 0.01758849355785175456 ),
 .UNSPECIFIED. ) ;
#3427=CARTESIAN_POINT ( 'NONE',  ( -3.318518101603116666, -7.321656987762883873, -8.399999999999991473 ) ) ;
#3432=ORIENTED_EDGE ( 'NONE', *, *, #1381, .T. ) ;
#3439=CARTESIAN_POINT ( 'NONE',  ( 5.080504117408890075, 2.106769544347818268, -8.400000000000018119 ) ) ;
#3465=CARTESIAN_POINT ( 'NONE',  ( 0.000000000000000000, 0.000000000000000000, 0.000000000000000000 ) ) ;
#3468=ORIENTED_EDGE ( 'NONE', *, *, #6930, .T. ) ;
#3470=CARTESIAN_POINT ( 'NONE',  ( 1.110223024625156540E-13, 9.237604307033992157, -0.7145311798163467287 ) ) ;
#3487=EDGE_CURVE ( 'NONE', #363, #6830, #6311, .T. ) ;
#3494=B_SPLINE_CURVE_WITH_KNOTS ( 'NONE', 3,
 ( #3378, #6061, #97, #5479, #4734, #193 ),
 .UNSPECIFIED., .F., .F.,
 ( 4, 2, 4 ),
 ( 0.008240550023493491139, 0.01057684187039397566, 0.01291313371729446019 ),
 .UNSPECIFIED. ) ;
#3505=EDGE_CURVE ( 'NONE', #6381, #5371, #5611, .T. ) ;
#3512=DIRECTION ( 'NONE',  ( 1.000000000000000000, 0.000000000000000000, 0.000000000000000000 ) ) ;
#3541=EDGE_CURVE ( 'NONE', #4330, #5371, #7136, .T. ) ;
#3544=ORIENTED_EDGE ( 'NONE', *, *, #1926, .T. ) ;
#3557=B_SPLINE_CURVE_WITH_KNOTS ( 'NONE', 3,
 ( #7219, #2649, #4700, #7346, #1383, #908, #2209, #5529 ),
 .UNSPECIFIED., .F., .F.,
 ( 4, 2, 2, 4 ),
 ( 0.004673709593152344799, 0.005837709341827777842, 0.007001709090503210886, 0.009329708587854076973 ),
 .UNSPECIFIED. ) ;
#3571=FACE_BOUND ( 'NONE', #5623, .T. ) ;
#3607=DIRECTION ( 'NONE',  ( 0.000000000000000000, 0.000000000000000000, -1.000000000000000000 ) ) ;
#3618=CARTESIAN_POINT ( 'NONE',  ( 0.000000000000000000, 0.000000000000000000, 0.000000000000000000 ) ) ;
#3619=EDGE_CURVE ( 'NONE', #8461, #1223, #6631, .T. ) ;
#3622=VERTEX_POINT ( 'NONE', #5094 ) ;
#3635=CARTESIAN_POINT ( 'NONE',  ( 5.080504117408890075, 2.106769544347818268, 0.000000000000000000 ) ) ;
#3650=ORIENTED_EDGE ( 'NONE', *, *, #8047, .F. ) ;
#3655=DIRECTION ( 'NONE',  ( 0.000000000000000000, 0.000000000000000000, -1.000000000000000000 ) ) ;
#3657=DIRECTION ( 'NONE',  ( 0.000000000000000000, 0.000000000000000000, 1.000000000000000000 ) ) ;
#3663=B_SPLINE_CURVE_WITH_KNOTS ( 'NONE', 3,
 ( #2992, #8269, #7569, #5488, #4301, #2210 ),
 .UNSPECIFIED., .F., .F.,
 ( 4, 2, 4 ),
 ( 0.008240550023493511955, 0.01057684187039398607, 0.01291313371729446192 ),
 .UNSPECIFIED. ) ;
#3686=CARTESIAN_POINT ( 'NONE',  ( 8.000000000000119016, 3.115336682266878654, -8.080606868608478877 ) ) ;
#3696=CYLINDRICAL_SURFACE ( 'NONE', #5816, 5.500000000000024869 ) ;
#3733=DIRECTION ( 'NONE',  ( 0.000000000000000000, 0.000000000000000000, 1.000000000000000000 ) ) ;
#3735=CIRCLE ( 'NONE', #8590, 8.000000000000007105 ) ;
#3745=ADVANCED_FACE ( 'NONE', ( #4675 ), #2714, .T. ) ;
#3754=FACE_OUTER_BOUND ( 'NONE', #3181, .T. ) ;
#3772=ORIENTED_EDGE ( 'NONE', *, *, #3619, .T. ) ;
#3776=DIRECTION ( 'NONE',  ( -0.9237280213470678847, -0.3830490080632384942, 0.000000000000000000 ) ) ;
#3796=ORIENTED_EDGE ( 'NONE', *, *, #6904, .T. ) ;
#3805=CARTESIAN_POINT ( 'NONE',  ( 8.000000000000122569, 0.7809653281574663319, -8.399999999999955946 ) ) ;
#3815=DIRECTION ( 'NONE',  ( 0.5000000000000035527, 0.8660254037844365982, 0.000000000000000000 ) ) ;
#3823=DIRECTION ( 'NONE',  ( -0.000000000000000000, -0.000000000000000000, 1.000000000000000000 ) ) ;
#3859=EDGE_CURVE ( 'NONE', #5854, #5405, #5610, .T. ) ;
#3881=FACE_OUTER_BOUND ( 'NONE', #7203, .T. ) ;
#3882=ORIENTED_EDGE ( 'NONE', *, *, #4088, .F. ) ;
#3909=ADVANCED_FACE ( 'NONE', ( #5027 ), #7985, .T. ) ;
#3910=VERTEX_POINT ( 'NONE', #7728 ) ;
#3915=AXIS2_PLACEMENT_3D ( 'NONE', #2481, #5631, #6232 ) ;
#3944=AXIS2_PLACEMENT_3D ( 'NONE', #7616, #1635, #6974 ) ;
#3946=CARTESIAN_POINT ( 'NONE',  ( 7.347286611337029427, 4.995646404165263732, -0.4969600502617758098 ) ) ;
#3957=CARTESIAN_POINT ( 'NONE',  ( 0.000000000000000000, 0.000000000000000000, -8.400000000000018119 ) ) ;
#3984=EDGE_CURVE ( 'NONE', #4330, #6381, #4446, .T. ) ;
#4010=DIRECTION ( 'NONE',  ( -0.5000000000000041078, 0.8660254037844363761, 0.000000000000000000 ) ) ;
#4026=CARTESIAN_POINT ( 'NONE',  ( -6.689127551062048482, -5.375634714784658819, -0.3173508448886869227 ) ) ;
#4054=CARTESIAN_POINT ( 'NONE',  ( 0.6527133886630634985, -8.860760056385847960, -0.4969600502618143900 ) ) ;
#4069=CARTESIAN_POINT ( 'NONE',  ( -8.000000000000000000, -3.098204225878153917, -0.3157906771918689848 ) ) ;
#4080=CARTESIAN_POINT ( 'NONE',  ( -4.000000000000003553, 6.928203230275431501, 0.000000000000000000 ) ) ;
#4081=DIRECTION ( 'NONE',  ( -1.000000000000000000, -8.881784197001244435E-16, 0.000000000000000000 ) ) ;
#4088=EDGE_CURVE ( 'NONE', #6543, #7164, #7263, .T. ) ;
#4092=ORIENTED_EDGE ( 'NONE', *, *, #5327, .F. ) ;
#4108=DIRECTION ( 'NONE',  ( -1.000000000000000000, -8.881784197001244435E-16, 0.000000000000000000 ) ) ;
#4115=DIRECTION ( 'NONE',  ( 0.000000000000000000, 0.000000000000000000, -1.000000000000000000 ) ) ;
#4118=CARTESIAN_POINT ( 'NONE',  ( -8.000000000000007105, -4.618802153517065356, -7.685468820183672278 ) ) ;
#4119=DIRECTION ( 'NONE',  ( -0.000000000000000000, -0.000000000000000000, 1.000000000000000000 ) ) ;
#4142=VERTEX_POINT ( 'NONE', #4118 ) ;
#4147=CARTESIAN_POINT ( 'NONE',  ( -3.660532965668796823, 7.124194613927540054, -8.400000000000076739 ) ) ;
#4148=DIRECTION ( 'NONE',  ( 0.8660254037844369313, 0.5000000000000028866, 0.000000000000000000 ) ) ;
#4188=CARTESIAN_POINT ( 'NONE',  ( 1.110223024625156540E-13, 9.237604307033992157, -7.685468820183672278 ) ) ;
#4203=CARTESIAN_POINT ( 'NONE',  ( 0.000000000000000000, 0.000000000000000000, 0.000000000000000000 ) ) ;
#4204=ORIENTED_EDGE ( 'NONE', *, *, #6495, .F. ) ;
#4208=PRODUCT_DEFINITION_CONTEXT ( 'detailed design', #6645, 'design' ) ;
#4230=DIRECTION ( 'NONE',  ( -1.000000000000000000, -8.881784197001244435E-16, 0.000000000000000000 ) ) ;
#4249=ORIENTED_EDGE ( 'NONE', *, *, #335, .T. ) ;
#4258=CARTESIAN_POINT ( 'NONE',  ( 0.000000000000000000, 0.000000000000000000, 0.000000000000000000 ) ) ;
#4265=EDGE_CURVE ( 'NONE', #4500, #2369, #2957, .T. ) ;
#4266=( GEOMETRIC_REPRESENTATION_CONTEXT ( 3 ) GLOBAL_UNCERTAINTY_ASSIGNED_CONTEXT ( ( #2346 ) ) GLOBAL_UNIT_ASSIGNED_CONTEXT ( ( #5167, #7870, #3211 ) ) REPRESENTATION_CONTEXT ( 'NONE', 'WORKASPACE' ) );
#4272=EDGE_CURVE ( 'NONE', #1627, #6142, #1333, .T. ) ;
#4283=ORIENTED_EDGE ( 'NONE', *, *, #2339, .T. ) ;
#4288=AXIS2_PLACEMENT_3D ( 'NONE', #7665, #1682, #4230 ) ;
#4297=AXIS2_PLACEMENT_3D ( 'NONE', #6087, #1450, #4108 ) ;
#4301=CARTESIAN_POINT ( 'NONE',  ( 8.000000000000122569, -0.7805016046292545528, -8.399999999999939959 ) ) ;
#4306=CARTESIAN_POINT ( 'NONE',  ( 0.000000000000000000, 0.000000000000000000, -8.400000000000018119 ) ) ;
#4311=DIRECTION ( 'NONE',  ( -1.000000000000000000, -8.881784197001244435E-16, 0.000000000000000000 ) ) ;
#4322=AXIS2_PLACEMENT_3D ( 'NONE', #2428, #7174, #4469 ) ;
#4330=VERTEX_POINT ( 'NONE', #7455 ) ;
#4343=CARTESIAN_POINT ( 'NONE',  ( 8.000000000000117240, 4.618802153516954334, -8.400000000000018119 ) ) ;
#4381=ORIENTED_EDGE ( 'NONE', *, *, #2217, .F. ) ;
#4395=EDGE_LOOP ( 'NONE', ( #2298, #6267, #1776 ) ) ;
#4422=CARTESIAN_POINT ( 'NONE',  ( 2.645508037661961520, 7.710219529346607814, -8.331901280394573561 ) ) ;
#4426=CARTESIAN_POINT ( 'NONE',  ( 4.000000000000114575, 6.928203230275597591, 0.000000000000000000 ) ) ;
#4446=B_SPLINE_CURVE_WITH_KNOTS ( 'NONE', 3,
 ( #7248, #1282, #5340, #7995, #1230, #4026, #5926, #584 ),
 .UNSPECIFIED., .F., .F.,
 ( 4, 2, 2, 4 ),
 ( 0.004673709593152344799, 0.005837709341827777842, 0.007001709090503210886, 0.009329708587854076973 ),
 .UNSPECIFIED. ) ;
#4450=CARTESIAN_POINT ( 'NONE',  ( 4.000000000000003553, -6.928203230275542523, -8.400000000000018119 ) ) ;
#4461=CARTESIAN_POINT ( 'NONE',  ( 1.110223024625156540E-13, 9.237604307033992157, -7.685468820183672278 ) ) ;
#4469=DIRECTION ( 'NONE',  ( -1.000000000000000000, -8.881784197001244435E-16, 0.000000000000000000 ) ) ;
#4484=AXIS2_PLACEMENT_3D ( 'NONE', #904, #760, #4771 ) ;
#4498=FACE_OUTER_BOUND ( 'NONE', #1946, .T. ) ;
#4500=VERTEX_POINT ( 'NONE', #1269 ) ;
#4585=CONICAL_SURFACE ( 'NONE', #2635, 8.000000000000007105, 1.047197551196597631 ) ;
#4596=CARTESIAN_POINT ( 'NONE',  ( -8.000000000000007105, 4.618802153517009401, -0.7145311798163467287 ) ) ;
#4612=CARTESIAN_POINT ( 'NONE',  ( -0.6543471694412738016, -8.859816792613717240, -0.4964154566688340764 ) ) ;
#4622=CARTESIAN_POINT ( 'NONE',  ( 8.000000000000007105, 4.618802153516899267, -0.7145311798163467287 ) ) ;
#4625=ORIENTED_EDGE ( 'NONE', *, *, #5607, .F. ) ;
#4646=AXIS2_PLACEMENT_3D ( 'NONE', #7751, #6985, #5648 ) ;
#4650=DIRECTION ( 'NONE',  ( -1.000000000000000000, -8.881784197001244435E-16, 0.000000000000000000 ) ) ;
#4671=CARTESIAN_POINT ( 'NONE',  ( -8.000000000000000000, -3.098204225878149920, -8.084209322808149523 ) ) ;
#4673=PRODUCT_DEFINITION ( 'UNKNOWN', '', #3259, #4208 ) ;
#4675=FACE_OUTER_BOUND ( 'NONE', #7828, .T. ) ;
#4688=AXIS2_PLACEMENT_3D ( 'NONE', #7250, #2025, #4689 ) ;
#4689=DIRECTION ( 'NONE',  ( 0.9237280213470678847, 0.3830490080632384942, 0.000000000000000000 ) ) ;
#4690=ADVANCED_FACE ( 'NONE', ( #1133, #3754 ), #6414, .T. ) ;
#4692=CARTESIAN_POINT ( 'NONE',  ( 0.000000000000000000, 0.000000000000000000, -8.400000000000018119 ) ) ;
#4694=ORIENTED_EDGE ( 'NONE', *, *, #535, .T. ) ;
#4697=DIRECTION ( 'NONE',  ( 0.9237280213470678847, 0.3830490080632384942, 0.000000000000000000 ) ) ;
#4700=CARTESIAN_POINT ( 'NONE',  ( -4.680456609904073417, -6.535341423375602865, -8.383111142572214902 ) ) ;
#4734=CARTESIAN_POINT ( 'NONE',  ( 8.000000000000120792, -0.7805016046292556631, -7.994805175954437918E-14 ) ) ;
#4743=CARTESIAN_POINT ( 'NONE',  ( -3.318518101603116666, -7.321656987762883873, -2.620211719036452669E-14 ) ) ;
#4761=EDGE_LOOP ( 'NONE', ( #3468, #7355, #7412 ) ) ;
#4763=EDGE_CURVE ( 'NONE', #6543, #6339, #5819, .T. ) ;
#4768=CARTESIAN_POINT ( 'NONE',  ( -7.999999999999785061, 4.618802153516870845, -7.685468820183672278 ) ) ;
#4771=DIRECTION ( 'NONE',  ( -1.000000000000000000, -8.881784197001244435E-16, 0.000000000000000000 ) ) ;
#4799=CARTESIAN_POINT ( 'NONE',  ( 2.644994884459147766, -7.710515798486462735, -0.08224679563977427277 ) ) ;
#4831=VERTEX_POINT ( 'NONE', #8492 ) ;
#4842=B_SPLINE_CURVE_WITH_KNOTS ( 'NONE', 3,
 ( #2836, #3354, #4671, #6629, #2752, #5992 ),
 .UNSPECIFIED., .F., .F.,
 ( 4, 2, 4 ),
 ( 0.008240550023493522364, 0.01057684187039419771, 0.01291313371729487305 ),
 .UNSPECIFIED. ) ;
#4853=FACE_OUTER_BOUND ( 'NONE', #1731, .T. ) ;
#4877=CARTESIAN_POINT ( 'NONE',  ( -8.000000000000001776, 0.7809653281576651729, -8.332263102140549280E-15 ) ) ;
#4891=ORIENTED_EDGE ( 'NONE', *, *, #5549, .F. ) ;
#4895=CYLINDRICAL_SURFACE ( 'NONE', #6581, 5.500000000000024869 ) ;
#4913=ORIENTED_EDGE ( 'NONE', *, *, #3984, .F. ) ;
#4923=ORIENTED_EDGE ( 'NONE', *, *, #2339, .F. ) ;
#4945=CARTESIAN_POINT ( 'NONE',  ( 3.318518101603081139, 7.321656987762871438, -8.400000000000003908 ) ) ;
#4953=CARTESIAN_POINT ( 'NONE',  ( 8.000000000000007105, -4.618802153517121312, -7.685468820183672278 ) ) ;
#4957=AXIS2_PLACEMENT_3D ( 'NONE', #2859, #6874, #6186 ) ;
#4959=DIRECTION ( 'NONE',  ( 0.000000000000000000, 0.000000000000000000, -1.000000000000000000 ) ) ;
#4960=VECTOR ( 'NONE', #1981, 1000.000000000000000 ) ;
#4997=ORIENTED_EDGE ( 'NONE', *, *, #133, .T. ) ;
#4999=FACE_OUTER_BOUND ( 'NONE', #6807, .T. ) ;
#5005=AXIS2_PLACEMENT_3D ( 'NONE', #4306, #3657, #1513 ) ;
#5020=DIRECTION ( 'NONE',  ( 0.000000000000000000, 0.000000000000000000, 1.000000000000000000 ) ) ;
#5027=FACE_OUTER_BOUND ( 'NONE', #4395, .T. ) ;
#5045=B_SPLINE_CURVE_WITH_KNOTS ( 'NONE', 3,
 ( #4080, #2735, #5390, #8089, #6828, #8043, #6745, #3470 ),
 .UNSPECIFIED., .F., .F.,
 ( 4, 2, 2, 4 ),
 ( 0.004673709593152062039, 0.005837709341827626922, 0.007001709090503191804, 0.009329708587854326773 ),
 .UNSPECIFIED. ) ;
#5057=CARTESIAN_POINT ( 'NONE',  ( 4.680456609904033449, 6.535341423375591319, -8.383111142572232666 ) ) ;
#5071=VECTOR ( 'NONE', #7022, 1000.000000000000000 ) ;
#5094=CARTESIAN_POINT ( 'NONE',  ( -4.000000000000003553, 6.928203230275431501, 0.000000000000000000 ) ) ;
#5099=FACE_OUTER_BOUND ( 'NONE', #6781, .T. ) ;
#5103=SHAPE_REPRESENTATION_RELATIONSHIP ( 'NONE' , 'NONE' ,  #3167, #212 ) ;
#5105=EDGE_CURVE ( 'NONE', #6936, #4831, #1235, .T. ) ;
#5137=VECTOR ( 'NONE', #5313, 1000.000000000000000 ) ;
#5162=ORIENTED_EDGE ( 'NONE', *, *, #8047, .T. ) ;
#5167=( LENGTH_UNIT ( ) NAMED_UNIT ( * ) SI_UNIT ( .MILLI., .METRE. ) );
#5208=CARTESIAN_POINT ( 'NONE',  ( 2.645508037661961520, 7.710219529346607814, -0.06809871960544289227 ) ) ;
#5249=CARTESIAN_POINT ( 'NONE',  ( 5.080504117408896292, 2.106769544347820933, -8.401000000000047763 ) ) ;
#5257=CARTESIAN_POINT ( 'NONE',  ( 0.000000000000000000, 0.000000000000000000, -8.400000000000018119 ) ) ;
#5275=CONICAL_SURFACE ( 'NONE', #4288, 8.000000000000007105, 1.047197551196597631 ) ;
#5301=CARTESIAN_POINT ( 'NONE',  ( 4.680456609904033449, 6.535341423375591319, -0.01688885742778744800 ) ) ;
#5313=DIRECTION ( 'NONE',  ( 0.000000000000000000, 0.000000000000000000, 1.000000000000000000 ) ) ;
#5318=CARTESIAN_POINT ( 'NONE',  ( 8.000000000000117240, 3.871967595402001194, -0.4989386132324870049 ) ) ;
#5327=EDGE_CURVE ( 'NONE', #6269, #7120, #5777, .T. ) ;
#5340=CARTESIAN_POINT ( 'NONE',  ( -4.680456609904073417, -6.535341423375602865, -0.01688885742780586036 ) ) ;
#5354=FACE_OUTER_BOUND ( 'NONE', #7647, .T. ) ;
#5371=VERTEX_POINT ( 'NONE', #487 ) ;
#5390=CARTESIAN_POINT ( 'NONE',  ( -3.319543390095988755, 7.321065037175355172, -0.01688885742771796192 ) ) ;
#5397=DIRECTION ( 'NONE',  ( -1.000000000000000000, -8.881784197001244435E-16, 0.000000000000000000 ) ) ;
#5405=VERTEX_POINT ( 'NONE', #400 ) ;
#5410=CARTESIAN_POINT ( 'NONE',  ( 3.660532965668853667, -7.124194613927719466, -5.559246639419425248E-14 ) ) ;
#5437=CARTESIAN_POINT ( 'NONE',  ( -4.000000000000114575, -6.928203230275487456, -8.400000000000018119 ) ) ;
#5479=CARTESIAN_POINT ( 'NONE',  ( 8.000000000000119016, -1.555946510856292209, -0.06708870216344244020 ) ) ;
#5488=CARTESIAN_POINT ( 'NONE',  ( 8.000000000000122569, -1.555946510856290210, -8.332911297836574249 ) ) ;
#5529=CARTESIAN_POINT ( 'NONE',  ( -8.000000000000007105, -4.618802153517065356, -7.685468820183672278 ) ) ;
#5549=EDGE_CURVE ( 'NONE', #5371, #3622, #1736, .T. ) ;
#5566=CARTESIAN_POINT ( 'NONE',  ( -0.6543471694412733575, -8.859816792613717240, -7.903584543331185763 ) ) ;
#5582=CARTESIAN_POINT ( 'NONE',  ( 4.000000000000003553, -6.928203230275542523, -8.400000000000018119 ) ) ;
#5590=EDGE_CURVE ( 'NONE', #6269, #3910, #2044, .T. ) ;
#5603=CARTESIAN_POINT ( 'NONE',  ( -8.000000000000005329, 3.115336682266933277, -8.080606868608525062 ) ) ;
#5607=EDGE_CURVE ( 'NONE', #1223, #6543, #3494, .T. ) ;
#5610=B_SPLINE_CURVE_WITH_KNOTS ( 'NONE', 3,
 ( #4461, #7648, #6430, #4422, #4945, #3157 ),
 .UNSPECIFIED., .F., .F.,
 ( 4, 2, 4 ),
 ( 2.380731629389045982E-07, 0.002336973833157555535, 0.004673709593152172194 ),
 .UNSPECIFIED. ) ;
#5611=B_SPLINE_CURVE_WITH_KNOTS ( 'NONE', 3,
 ( #6782, #1417, #4069, #8591, #806, #6007 ),
 .UNSPECIFIED., .F., .F.,
 ( 4, 2, 4 ),
 ( 0.008240550023493515425, 0.01057684187039419250, 0.01291313371729486958 ),
 .UNSPECIFIED. ) ;
#5620=EDGE_CURVE ( 'NONE', #3622, #2009, #5045, .T. ) ;
#5623=EDGE_LOOP ( 'NONE', ( #1602, #7323 ) ) ;
#5631=DIRECTION ( 'NONE',  ( 0.000000000000000000, 0.000000000000000000, 1.000000000000000000 ) ) ;
#5641=ORIENTED_EDGE ( 'NONE', *, *, #5105, .T. ) ;
#5648=DIRECTION ( 'NONE',  ( -1.000000000000000000, -8.881784197001244435E-16, -0.000000000000000000 ) ) ;
#5655=DIRECTION ( 'NONE',  ( 0.5000000000000029976, -0.8660254037844370423, 0.000000000000000000 ) ) ;
#5660=CARTESIAN_POINT ( 'NONE',  ( -7.999999999999785061, 4.618802153516870845, -7.685468820183672278 ) ) ;
#5684=MECHANICAL_DESIGN_GEOMETRIC_PRESENTATION_REPRESENTATION('',(#5820),#4266);
#5685=MANIFOLD_SOLID_BREP ( 'EndChamfer', #1111 ) ;
#5709=DIRECTION ( 'NONE',  ( 0.000000000000000000, 0.000000000000000000, 1.000000000000000000 ) ) ;
#5710=( LENGTH_UNIT ( ) NAMED_UNIT ( * ) SI_UNIT ( .MILLI., .METRE. ) );
#5715=DIRECTION ( 'NONE',  ( 0.000000000000000000, 0.000000000000000000, 1.000000000000000000 ) ) ;
#5727=ORIENTED_EDGE ( 'NONE', *, *, #6479, .F. ) ;
#5739=CONICAL_SURFACE ( 'NONE', #1955, 8.000000000000007105, 1.047197551196597631 ) ;
#5759=CARTESIAN_POINT ( 'NONE',  ( -7.999999999999785061, 4.618802153516870845, -7.685468820183672278 ) ) ;
#5770=CARTESIAN_POINT ( 'NONE',  ( 8.000000000000007105, -4.618802153517121312, -0.7145311798163467287 ) ) ;
#5777=LINE ( 'NONE', #7104, #5071 ) ;
#5783=CARTESIAN_POINT ( 'NONE',  ( 8.000000000000007105, 4.618802153516899267, -0.7145311798163467287 ) ) ;
#5788=CARTESIAN_POINT ( 'NONE',  ( 7.347286611337029427, 4.995646404165263732, -7.903039949738243308 ) ) ;
#5796=ADVANCED_FACE ( 'NONE', ( #5354 ), #5739, .T. ) ;
#5815=ORIENTED_EDGE ( 'NONE', *, *, #3859, .F. ) ;
#5816=AXIS2_PLACEMENT_3D ( 'NONE', #385, #3733, #3776 ) ;
#5819=B_SPLINE_CURVE_WITH_KNOTS ( 'NONE', 3,
 ( #7973, #2006, #7276, #6578, #5318, #4622 ),
 .UNSPECIFIED., .F., .F.,
 ( 4, 2, 4 ),
 ( 0.01291313371729446019, 0.01525081363757301890, 0.01758849355785157761 ),
 .UNSPECIFIED. ) ;
#5820=STYLED_ITEM('',(#8670),#5685);
#5854=VERTEX_POINT ( 'NONE', #1764 ) ;
#5868=CONICAL_SURFACE ( 'NONE', #5005, 8.000000000000007105, 1.047197551196597631 ) ;
#5880=ADVANCED_FACE ( 'NONE', ( #1155 ), #1078, .T. ) ;
#5887=CARTESIAN_POINT ( 'NONE',  ( 1.110223024625156540E-13, 9.237604307033992157, -0.7145311798163467287 ) ) ;
#5894=EDGE_LOOP ( 'NONE', ( #557, #847, #4997, #373 ) ) ;
#5919=CARTESIAN_POINT ( 'NONE',  ( 0.000000000000000000, 0.000000000000000000, -8.400000000000018119 ) ) ;
#5926=CARTESIAN_POINT ( 'NONE',  ( -7.347286611336995676, -4.995646404165323240, -0.4969600502617779747 ) ) ;
#5953=ORIENTED_EDGE ( 'NONE', *, *, #8008, .T. ) ;
#5976=DIRECTION ( 'NONE',  ( 0.000000000000000000, 0.000000000000000000, 1.000000000000000000 ) ) ;
#5984=ORIENTED_EDGE ( 'NONE', *, *, #2217, .T. ) ;
#5992=CARTESIAN_POINT ( 'NONE',  ( -8.000000000000007105, 1.110223024625156540E-13, -8.400000000000018119 ) ) ;
#5993=DIRECTION ( 'NONE',  ( 0.000000000000000000, 0.000000000000000000, 1.000000000000000000 ) ) ;
#5997=AXIS2_PLACEMENT_3D ( 'NONE', #1615, #5655, #4148 ) ;
#6007=CARTESIAN_POINT ( 'NONE',  ( -8.000000000000007105, 1.110223024625156540E-13, 0.000000000000000000 ) ) ;
#6018=DIRECTION ( 'NONE',  ( -0.000000000000000000, -0.000000000000000000, 1.000000000000000000 ) ) ;
#6019=CARTESIAN_POINT ( 'NONE',  ( 8.000000000000117240, 4.618802153516954334, -8.400000000000018119 ) ) ;
#6036=ORIENTED_EDGE ( 'NONE', *, *, #485, .F. ) ;
#6037=DIRECTION ( 'NONE',  ( -0.8660254037844362651, -0.5000000000000039968, 0.000000000000000000 ) ) ;
#6042=CIRCLE ( 'NONE', #7269, 8.000000000000007105 ) ;
#6049=ORIENTED_EDGE ( 'NONE', *, *, #4265, .T. ) ;
#6057=CIRCLE ( 'NONE', #8121, 8.000000000000007105 ) ;
#6060=DIRECTION ( 'NONE',  ( 1.000000000000000000, 8.881784197001244435E-16, 0.000000000000000000 ) ) ;
#6061=CARTESIAN_POINT ( 'NONE',  ( 8.000000000000124345, -3.867591403079279733, -0.4976753153246756822 ) ) ;
#6076=ORIENTED_EDGE ( 'NONE', *, *, #4763, .T. ) ;
#6087=CARTESIAN_POINT ( 'NONE',  ( 0.000000000000000000, 0.000000000000000000, 0.000000000000000000 ) ) ;
#6098=ORIENTED_EDGE ( 'NONE', *, *, #5607, .T. ) ;
#6128=ORIENTED_EDGE ( 'NONE', *, *, #494, .F. ) ;
#6139=DIRECTION ( 'NONE',  ( 0.8660254037844367092, -0.5000000000000033307, 0.000000000000000000 ) ) ;
#6142=VERTEX_POINT ( 'NONE', #8286 ) ;
#6161=ORIENTED_EDGE ( 'NONE', *, *, #3303, .T. ) ;
#6186=DIRECTION ( 'NONE',  ( -1.000000000000000000, -8.881784197001244435E-16, 0.000000000000000000 ) ) ;
#6216=CARTESIAN_POINT ( 'NONE',  ( -0.6527133886629282733, 8.860760056385709404, -7.903039949738286829 ) ) ;
#6232=DIRECTION ( 'NONE',  ( -0.9237280213470678847, -0.3830490080632384942, 0.000000000000000000 ) ) ;
#6236=FACE_OUTER_BOUND ( 'NONE', #6822, .T. ) ;
#6267=ORIENTED_EDGE ( 'NONE', *, *, #3487, .T. ) ;
#6269=VERTEX_POINT ( 'NONE', #8534 ) ;
#6293=ORIENTED_EDGE ( 'NONE', *, *, #2683, .F. ) ;
#6311=CIRCLE ( 'NONE', #4484, 8.000000000000007105 ) ;
#6327=ORIENTED_EDGE ( 'NONE', *, *, #1294, .F. ) ;
#6329=B_SPLINE_CURVE_WITH_KNOTS ( 'NONE', 3,
 ( #375, #3805, #3022, #3686, #417, #1708 ),
 .UNSPECIFIED., .F., .F.,
 ( 4, 2, 4 ),
 ( 0.01291313371729446192, 0.01525081363757301717, 0.01758849355785157068 ),
 .UNSPECIFIED. ) ;
#6338=LINE ( 'NONE', #361, #8060 ) ;
#6339=VERTEX_POINT ( 'NONE', #5783 ) ;
#6350=B_SPLINE_CURVE_WITH_KNOTS ( 'NONE', 3,
 ( #2196, #314, #2976, #5603, #1577, #4768 ),
 .UNSPECIFIED., .F., .F.,
 ( 4, 2, 4 ),
 ( 0.01291313371729487305, 0.01525081363757324442, 0.01758849355785161578 ),
 .UNSPECIFIED. ) ;
#6374=CARTESIAN_POINT ( 'NONE',  ( 8.000000000000229150, -1.665334536937734811E-13, 0.000000000000000000 ) ) ;
#6381=VERTEX_POINT ( 'NONE', #567 ) ;
#6414=PLANE ( 'NONE',  #4646 ) ;
#6430=CARTESIAN_POINT ( 'NONE',  ( 1.313474075707311117, 8.479269695850856436, -8.083279549040174317 ) ) ;
#6479=EDGE_CURVE ( 'NONE', #4142, #92, #4842, .T. ) ;
#6491=CARTESIAN_POINT ( 'NONE',  ( 8.000000000000007105, -4.618802153517121312, -8.400000000000018119 ) ) ;
#6495=EDGE_CURVE ( 'NONE', #462, #7120, #2035, .T. ) ;
#6500=PLANE ( 'NONE',  #123 ) ;
#6519=DIRECTION ( 'NONE',  ( -1.000000000000000000, -7.194245199571014382E-14, 0.000000000000000000 ) ) ;
#6543=VERTEX_POINT ( 'NONE', #6374 ) ;
#6547=ADVANCED_FACE ( 'NONE', ( #4999 ), #5275, .T. ) ;
#6555=DIRECTION ( 'NONE',  ( -1.000000000000000000, -4.440892098500625373E-15, 0.000000000000000000 ) ) ;
#6565=CARTESIAN_POINT ( 'NONE',  ( -6.686525924292766376, 5.377136764700066074, -0.3167204509597931761 ) ) ;
#6578=CARTESIAN_POINT ( 'NONE',  ( 8.000000000000119016, 3.115336682266876434, -0.3193931313915404635 ) ) ;
#6581=AXIS2_PLACEMENT_3D ( 'NONE', #764, #3421, #809 ) ;
#6606=CARTESIAN_POINT ( 'NONE',  ( 5.690023276062453839, 5.952467836904148157, -0.1306530452038311141 ) ) ;
#6618=CARTESIAN_POINT ( 'NONE',  ( 5.354491962338145505, -6.146186931204510984, -0.06809871960548105618 ) ) ;
#6629=CARTESIAN_POINT ( 'NONE',  ( -7.999999999999998224, -1.555946510856075493, -8.332911297836668396 ) ) ;
#6631=LINE ( 'NONE', #6491, #174 ) ;
#6645=APPLICATION_CONTEXT ( 'automotive_design' ) ;
#6650=AXIS2_PLACEMENT_3D ( 'NONE', #1621, #1499, #6139 ) ;
#6669=CIRCLE ( 'NONE', #7767, 8.000000000000007105 ) ;
#6672=CARTESIAN_POINT ( 'NONE',  ( 1.310872448938031454, -8.480771745766503500, -0.3173508448887171207 ) ) ;
#6737=DIRECTION ( 'NONE',  ( 0.000000000000000000, 0.000000000000000000, 1.000000000000000000 ) ) ;
#6744=FACE_OUTER_BOUND ( 'NONE', #7939, .T. ) ;
#6745=CARTESIAN_POINT ( 'NONE',  ( -0.6527133886629282733, 8.860760056385709404, -0.4969600502617304016 ) ) ;
#6747=DIRECTION ( 'NONE',  ( 0.000000000000000000, 0.000000000000000000, -1.000000000000000000 ) ) ;
#6757=CARTESIAN_POINT ( 'NONE',  ( 7.345652830558768720, -4.996589667937484158, -0.4964154566688325776 ) ) ;
#6761=ORIENTED_EDGE ( 'NONE', *, *, #7578, .T. ) ;
#6781=EDGE_LOOP ( 'NONE', ( #5953, #2918, #6884 ) ) ;
#6782=CARTESIAN_POINT ( 'NONE',  ( -8.000000000000007105, -4.618802153517065356, -0.7145311798163467287 ) ) ;
#6786=FACE_OUTER_BOUND ( 'NONE', #6932, .T. ) ;
#6798=AXIS2_PLACEMENT_3D ( 'NONE', #243, #288, #2947 ) ;
#6807=EDGE_LOOP ( 'NONE', ( #6098, #5984, #1619 ) ) ;
#6822=EDGE_LOOP ( 'NONE', ( #4891, #1451, #3016, #4381, #2150, #2944 ) ) ;
#6828=CARTESIAN_POINT ( 'NONE',  ( -2.309976723937542609, 7.903938623646810768, -0.1306530452037677759 ) ) ;
#6830=VERTEX_POINT ( 'NONE', #556 ) ;
#6874=DIRECTION ( 'NONE',  ( 0.000000000000000000, 0.000000000000000000, -1.000000000000000000 ) ) ;
#6880=FACE_OUTER_BOUND ( 'NONE', #4761, .T. ) ;
#6884=ORIENTED_EDGE ( 'NONE', *, *, #7306, .T. ) ;
#6888=CARTESIAN_POINT ( 'NONE',  ( -8.000000000000005329, 3.115336682267020763, -0.3193931313915108761 ) ) ;
#6904=EDGE_CURVE ( 'NONE', #1223, #462, #7947, .T. ) ;
#6907=B_SPLINE_CURVE_WITH_KNOTS ( 'NONE', 3,
 ( #7436, #2130, #5301, #2030, #6606, #2736, #3946, #7255 ),
 .UNSPECIFIED., .F., .F.,
 ( 4, 2, 2, 4 ),
 ( 0.004673709593152171327, 0.005837709341827673759, 0.007001709090503176192, 0.009329708587854181057 ),
 .UNSPECIFIED. ) ;
#6908=ORIENTED_EDGE ( 'NONE', *, *, #1100, .T. ) ;
#6920=VECTOR ( 'NONE', #7902, 1000.000000000000000 ) ;
#6928=FACE_OUTER_BOUND ( 'NONE', #2200, .T. ) ;
#6930=EDGE_CURVE ( 'NONE', #3622, #7164, #6669, .T. ) ;
#6932=EDGE_LOOP ( 'NONE', ( #2928, #3133, #1324, #6049 ) ) ;
#6936=VERTEX_POINT ( 'NONE', #3439 ) ;
#6943=CARTESIAN_POINT ( 'NONE',  ( 0.6527133886630634985, -8.860760056385847960, -7.903039949738205117 ) ) ;
#6948=AXIS2_PLACEMENT_3D ( 'NONE', #5919, #84, #754 ) ;
#6961=CIRCLE ( 'NONE', #7506, 8.000000000000007105 ) ;
#6974=DIRECTION ( 'NONE',  ( -1.000000000000000000, -8.881784197001244435E-16, -0.000000000000000000 ) ) ;
#6981=EDGE_CURVE ( 'NONE', #8461, #363, #890, .T. ) ;
#6985=DIRECTION ( 'NONE',  ( 0.000000000000000000, 0.000000000000000000, -1.000000000000000000 ) ) ;
#7011=DIRECTION ( 'NONE',  ( -0.8660254037844365982, 0.5000000000000035527, -0.000000000000000000 ) ) ;
#7022=DIRECTION ( 'NONE',  ( 0.000000000000000000, 0.000000000000000000, 1.000000000000000000 ) ) ;
#7029=PRODUCT_DEFINITION_SHAPE ( 'NONE', 'NONE',  #4673 ) ;
#7032=PRODUCT_CONTEXT ( 'NONE', #8190, 'mechanical' ) ;
#7035=CARTESIAN_POINT ( 'NONE',  ( 0.000000000000000000, 0.000000000000000000, 0.000000000000000000 ) ) ;
#7044=FACE_OUTER_BOUND ( 'NONE', #5894, .T. ) ;
#7071=CARTESIAN_POINT ( 'NONE',  ( -6.686525924292697098, 5.377136764700106930, -8.083279549040241818 ) ) ;
#7076=( NAMED_UNIT ( * ) SI_UNIT ( $, .STERADIAN. ) SOLID_ANGLE_UNIT ( ) );
#7086=CARTESIAN_POINT ( 'NONE',  ( 3.318518101603081139, 7.321656987762871438, -1.409124011052254044E-14 ) ) ;
#7104=CARTESIAN_POINT ( 'NONE',  ( 1.110223024625156540E-13, -9.237604307034075646, -8.400000000000018119 ) ) ;
#7120=VERTEX_POINT ( 'NONE', #8437 ) ;
#7122=ORIENTED_EDGE ( 'NONE', *, *, #4272, .T. ) ;
#7136=CIRCLE ( 'NONE', #8252, 8.000000000000007105 ) ;
#7141=ORIENTED_EDGE ( 'NONE', *, *, #485, .T. ) ;
#7164=VERTEX_POINT ( 'NONE', #4426 ) ;
#7174=DIRECTION ( 'NONE',  ( 0.000000000000000000, 0.000000000000000000, -1.000000000000000000 ) ) ;
#7177=CONICAL_SURFACE ( 'NONE', #2581, 8.000000000000007105, 1.047197551196597631 ) ;
#7193=CARTESIAN_POINT ( 'NONE',  ( -7.999999999999896083, -4.618802153517121312, -8.400000000000018119 ) ) ;
#7203=EDGE_LOOP ( 'NONE', ( #7122, #6908, #1590 ) ) ;
#7219=CARTESIAN_POINT ( 'NONE',  ( -4.000000000000114575, -6.928203230275487456, -8.400000000000018119 ) ) ;
#7228=DIRECTION ( 'NONE',  ( -0.9237280213470678847, -0.3830490080632384942, 0.000000000000000000 ) ) ;
#7248=CARTESIAN_POINT ( 'NONE',  ( -4.000000000000114575, -6.928203230275487456, 0.000000000000000000 ) ) ;
#7250=CARTESIAN_POINT ( 'NONE',  ( 0.000000000000000000, 0.000000000000000000, -8.400000000000018119 ) ) ;
#7255=CARTESIAN_POINT ( 'NONE',  ( 8.000000000000007105, 4.618802153516899267, -0.7145311798163467287 ) ) ;
#7260=CARTESIAN_POINT ( 'NONE',  ( -2.645508037661968181, -7.710219529346637124, -0.06809871960545786640 ) ) ;
#7263=CIRCLE ( 'NONE', #2002, 8.000000000000007105 ) ;
#7267=ADVANCED_FACE ( 'NONE', ( #7385 ), #1389, .T. ) ;
#7269=AXIS2_PLACEMENT_3D ( 'NONE', #2832, #8146, #874 ) ;
#7276=CARTESIAN_POINT ( 'NONE',  ( 8.000000000000120792, 1.572549600175473516, -0.06894455525518324024 ) ) ;
#7284=ADVANCED_FACE ( 'NONE', ( #6744 ), #4585, .T. ) ;
#7299=CARTESIAN_POINT ( 'NONE',  ( -8.000000000000007105, 4.618802153517009401, -0.7145311798163467287 ) ) ;
#7306=EDGE_CURVE ( 'NONE', #5405, #6142, #6961, .T. ) ;
#7307=FACE_OUTER_BOUND ( 'NONE', #1970, .T. ) ;
#7321=CARTESIAN_POINT ( 'NONE',  ( 4.000000000000003553, -6.928203230275542523, 0.000000000000000000 ) ) ;
#7323=ORIENTED_EDGE ( 'NONE', *, *, #133, .F. ) ;
#7324=CARTESIAN_POINT ( 'NONE',  ( 1.110223024625156540E-13, 9.237604307033992157, -8.400000000000018119 ) ) ;
#7346=CARTESIAN_POINT ( 'NONE',  ( -5.355005115540977911, -6.145890662064671162, -8.317753204360263553 ) ) ;
#7355=ORIENTED_EDGE ( 'NONE', *, *, #335, .F. ) ;
#7363=B_SPLINE_CURVE_WITH_KNOTS ( 'NONE', 3,
 ( #7468, #4147, #8160, #2195, #7505, #1531, #6216, #4188 ),
 .UNSPECIFIED., .F., .F.,
 ( 4, 2, 2, 4 ),
 ( 0.004673709593152062039, 0.005837709341827626922, 0.007001709090503191804, 0.009329708587854326773 ),
 .UNSPECIFIED. ) ;
#7385=FACE_OUTER_BOUND ( 'NONE', #8250, .T. ) ;
#7390=VERTEX_POINT ( 'NONE', #7299 ) ;
#7395=CARTESIAN_POINT ( 'NONE',  ( 6.686525924292801903, -5.377136764700267690, -0.3167204509598827156 ) ) ;
#7412=ORIENTED_EDGE ( 'NONE', *, *, #5620, .F. ) ;
#7436=CARTESIAN_POINT ( 'NONE',  ( 4.000000000000114575, 6.928203230275597591, 0.000000000000000000 ) ) ;
#7455=CARTESIAN_POINT ( 'NONE',  ( -4.000000000000114575, -6.928203230275487456, 0.000000000000000000 ) ) ;
#7466=ORIENTED_EDGE ( 'NONE', *, *, #8539, .F. ) ;
#7468=CARTESIAN_POINT ( 'NONE',  ( -4.000000000000003553, 6.928203230275431501, -8.400000000000018119 ) ) ;
#7478=DIRECTION ( 'NONE',  ( 0.000000000000000000, 0.000000000000000000, 1.000000000000000000 ) ) ;
#7480=B_SPLINE_CURVE_WITH_KNOTS ( 'NONE', 3,
 ( #406, #3057, #5057, #7715, #1744, #3096, #5788, #3394 ),
 .UNSPECIFIED., .F., .F.,
 ( 4, 2, 2, 4 ),
 ( 0.004673709593152172194, 0.005837709341827674626, 0.007001709090503176192, 0.009329708587854181057 ),
 .UNSPECIFIED. ) ;
#7488=CARTESIAN_POINT ( 'NONE',  ( 6.686525924292801903, -5.377136764700267690, -8.083279549040137013 ) ) ;
#7505=CARTESIAN_POINT ( 'NONE',  ( -2.309976723937542609, 7.903938623646810768, -8.269346954796251481 ) ) ;
#7506=AXIS2_PLACEMENT_3D ( 'NONE', #4692, #8552, #6555 ) ;
#7507=FACE_OUTER_BOUND ( 'NONE', #8592, .T. ) ;
#7563=AXIS2_PLACEMENT_3D ( 'NONE', #4203, #7478, #3512 ) ;
#7569=CARTESIAN_POINT ( 'NONE',  ( 8.000000000000126121, -3.098204225878304907, -8.084209322808050047 ) ) ;
#7578=EDGE_CURVE ( 'NONE', #2192, #6339, #3108, .T. ) ;
#7583=ORIENTED_EDGE ( 'NONE', *, *, #5327, .T. ) ;
#7590=PLANE ( 'NONE',  #5997 ) ;
#7616=CARTESIAN_POINT ( 'NONE',  ( 1.110223024625156540E-13, 9.237604307033992157, 0.000000000000000000 ) ) ;
#7620=EDGE_CURVE ( 'NONE', #6830, #2192, #6329, .T. ) ;
#7625=ORIENTED_EDGE ( 'NONE', *, *, #1714, .T. ) ;
#7647=EDGE_LOOP ( 'NONE', ( #5162, #465, #920 ) ) ;
#7648=CARTESIAN_POINT ( 'NONE',  ( 0.6543471694413474093, 8.859816792613639080, -7.903584543331222179 ) ) ;
#7662=FACE_OUTER_BOUND ( 'NONE', #2454, .T. ) ;
#7665=CARTESIAN_POINT ( 'NONE',  ( 0.000000000000000000, 0.000000000000000000, 0.000000000000000000 ) ) ;
#7678=SHAPE_DEFINITION_REPRESENTATION ( #7029, #3167 ) ;
#7715=CARTESIAN_POINT ( 'NONE',  ( 5.355005115540955707, 6.145890662064649845, -8.317753204360281316 ) ) ;
#7728=CARTESIAN_POINT ( 'NONE',  ( -4.000000000000114575, -6.928203230275487456, -8.400000000000018119 ) ) ;
#7731=CARTESIAN_POINT ( 'NONE',  ( 1.313474075707311339, 8.479269695850856436, -0.3167204509598462447 ) ) ;
#7751=CARTESIAN_POINT ( 'NONE',  ( 1.110223024625156540E-13, 9.237604307033992157, -8.400000000000018119 ) ) ;
#7756=CARTESIAN_POINT ( 'NONE',  ( 2.309976723937648746, -7.903938623646967088, -8.269346954796146676 ) ) ;
#7767=AXIS2_PLACEMENT_3D ( 'NONE', #3298, #1303, #781 ) ;
#7805=ORIENTED_EDGE ( 'NONE', *, *, #1294, .T. ) ;
#7828=EDGE_LOOP ( 'NONE', ( #8213, #7805, #8330, #4923, #1378, #8166 ) ) ;
#7835=CONICAL_SURFACE ( 'NONE', #331, 8.000000000000007105, 1.047197551196597631 ) ;
#7853=PRODUCT ( 'hex nut style 1_am_B18.2.4.1M - Hex nut, Style 1,  M10 x 1.5, with 16mm WAF --D-N', 'hex nut style 1_am_B18.2.4.1M - Hex nut, Style 1,  M10 x 1.5, with 16mm WAF --D-N', '', ( #7032 ) ) ;
#7859=AXIS2_PLACEMENT_3D ( 'NONE', #6019, #5397, #14 ) ;
#7870=( NAMED_UNIT ( * ) PLANE_ANGLE_UNIT ( ) SI_UNIT ( $, .RADIAN. ) );
#7902=DIRECTION ( 'NONE',  ( 0.000000000000000000, 0.000000000000000000, 1.000000000000000000 ) ) ;
#7911=B_SPLINE_CURVE_WITH_KNOTS ( 'NONE', 3,
 ( #5887, #8510, #7731, #5208, #7086, #1765 ),
 .UNSPECIFIED., .F., .F.,
 ( 4, 2, 4 ),
 ( 2.380731629388737080E-07, 0.002336973833157555101, 0.004673709593152171327 ),
 .UNSPECIFIED. ) ;
#7914=EDGE_LOOP ( 'NONE', ( #2566, #1547, #6327 ) ) ;
#7921=ORIENTED_EDGE ( 'NONE', *, *, #1926, .F. ) ;
#7939=EDGE_LOOP ( 'NONE', ( #1956, #6036, #4204 ) ) ;
#7947=B_SPLINE_CURVE_WITH_KNOTS ( 'NONE', 3,
 ( #8565, #6757, #7395, #6618, #8098, #2698 ),
 .UNSPECIFIED., .F., .F.,
 ( 4, 2, 4 ),
 ( 2.380731629386716377E-07, 0.002336973833157600638, 0.004673709593152262400 ),
 .UNSPECIFIED. ) ;
#7953=FACE_OUTER_BOUND ( 'NONE', #7914, .T. ) ;
#7973=CARTESIAN_POINT ( 'NONE',  ( 8.000000000000229150, -1.665334536937734811E-13, 0.000000000000000000 ) ) ;
#7985=CONICAL_SURFACE ( 'NONE', #168, 8.000000000000007105, 1.047197551196597631 ) ;
#7995=CARTESIAN_POINT ( 'NONE',  ( -5.355005115540977911, -6.145890662064671162, -0.08224679563975283159 ) ) ;
#8006=DIRECTION ( 'NONE',  ( 1.000000000000000000, 8.881784197001244435E-16, 0.000000000000000000 ) ) ;
#8008=EDGE_CURVE ( 'NONE', #6142, #5854, #7363, .T. ) ;
#8043=CARTESIAN_POINT ( 'NONE',  ( -1.310872448937907997, 8.480771745766357839, -0.3173508448886235289 ) ) ;
#8046=CARTESIAN_POINT ( 'NONE',  ( 0.000000000000000000, -9.237604307034075646, -0.7145311798163467287 ) ) ;
#8047=EDGE_CURVE ( 'NONE', #363, #6269, #1035, .T. ) ;
#8060=VECTOR ( 'NONE', #2441, 1000.000000000000000 ) ;
#8062=CARTESIAN_POINT ( 'NONE',  ( 0.000000000000000000, -9.237604307034075646, -0.7145311798163467287 ) ) ;
#8070=VECTOR ( 'NONE', #8460, 1000.000000000000000 ) ;
#8089=CARTESIAN_POINT ( 'NONE',  ( -2.644994884459048290, 7.710515798486305528, -0.08224679563966873219 ) ) ;
#8091=ORIENTED_EDGE ( 'NONE', *, *, #4763, .F. ) ;
#8098=CARTESIAN_POINT ( 'NONE',  ( 4.681481898397022334, -6.534749472788251801, -5.280064580004406594E-14 ) ) ;
#8117=CARTESIAN_POINT ( 'NONE',  ( 8.000000000000007105, 4.618802153516899267, -7.685468820183672278 ) ) ;
#8121=AXIS2_PLACEMENT_3D ( 'NONE', #1051, #3823, #6519 ) ;
#8139=CARTESIAN_POINT ( 'NONE',  ( 7.345652830558768720, -4.996589667937484158, -7.903584543331182211 ) ) ;
#8146=DIRECTION ( 'NONE',  ( -0.000000000000000000, -0.000000000000000000, 1.000000000000000000 ) ) ;
#8153=EDGE_CURVE ( 'NONE', #5405, #2192, #7480, .T. ) ;
#8160=CARTESIAN_POINT ( 'NONE',  ( -3.319543390095988755, 7.321065037175355172, -8.383111142572301944 ) ) ;
#8166=ORIENTED_EDGE ( 'NONE', *, *, #4272, .F. ) ;
#8190=APPLICATION_CONTEXT ( 'automotive_design' ) ;
#8213=ORIENTED_EDGE ( 'NONE', *, *, #2683, .T. ) ;
#8216=CARTESIAN_POINT ( 'NONE',  ( -2.645508037661968181, -7.710219529346637124, -8.331901280394562903 ) ) ;
#8228=CARTESIAN_POINT ( 'NONE',  ( 4.681481898397022334, -6.534749472788251801, -8.399999999999964828 ) ) ;
#8234=VECTOR ( 'NONE', #5993, 1000.000000000000000 ) ;
#8242=AXIS2_PLACEMENT_3D ( 'NONE', #1632, #3655, #342 ) ;
#8250=EDGE_LOOP ( 'NONE', ( #1871, #8589, #4694 ) ) ;
#8252=AXIS2_PLACEMENT_3D ( 'NONE', #628, #4115, #1458 ) ;
#8269=CARTESIAN_POINT ( 'NONE',  ( 8.000000000000126121, -3.867591403079282397, -7.902324684675341437 ) ) ;
#8272=PLANE ( 'NONE',  #3944 ) ;
#8286=CARTESIAN_POINT ( 'NONE',  ( -4.000000000000003553, 6.928203230275431501, -8.400000000000018119 ) ) ;
#8296=ADVANCED_FACE ( 'NONE', ( #6928 ), #5868, .T. ) ;
#8330=ORIENTED_EDGE ( 'NONE', *, *, #5620, .T. ) ;
#8331=AXIS2_PLACEMENT_3D ( 'NONE', #371, #5020, #1750 ) ;
#8345=DIRECTION ( 'NONE',  ( 1.000000000000000000, 8.881784197001244435E-16, 0.000000000000000000 ) ) ;
#8383=( NAMED_UNIT ( * ) PLANE_ANGLE_UNIT ( ) SI_UNIT ( $, .RADIAN. ) );
#8392=ADVANCED_FACE ( 'NONE', ( #3571, #6236 ), #8272, .F. ) ;
#8410=CARTESIAN_POINT ( 'NONE',  ( -4.000000000000114575, -6.928203230275487456, 0.000000000000000000 ) ) ;
#8437=CARTESIAN_POINT ( 'NONE',  ( 0.000000000000000000, -9.237604307034075646, -0.7145311798163467287 ) ) ;
#8453=CARTESIAN_POINT ( 'NONE',  ( 3.660532965668853667, -7.124194613927719466, -8.399999999999964828 ) ) ;
#8458=ORIENTED_EDGE ( 'NONE', *, *, #6479, .T. ) ;
#8460=DIRECTION ( 'NONE',  ( 0.000000000000000000, 0.000000000000000000, 1.000000000000000000 ) ) ;
#8461=VERTEX_POINT ( 'NONE', #1724 ) ;
#8492=CARTESIAN_POINT ( 'NONE',  ( -5.080504117408890075, -2.106769544347818712, -8.400000000000018119 ) ) ;
#8501=DIRECTION ( 'NONE',  ( -1.000000000000000000, -8.881784197001244435E-16, 0.000000000000000000 ) ) ;
#8510=CARTESIAN_POINT ( 'NONE',  ( 0.6543471694413475204, 8.859816792613639080, -0.4964154566687958292 ) ) ;
#8534=CARTESIAN_POINT ( 'NONE',  ( 0.000000000000000000, -9.237604307034075646, -7.685468820183672278 ) ) ;
#8539=EDGE_CURVE ( 'NONE', #7164, #6339, #6907, .T. ) ;
#8552=DIRECTION ( 'NONE',  ( -0.000000000000000000, -0.000000000000000000, 1.000000000000000000 ) ) ;
#8563=CARTESIAN_POINT ( 'NONE',  ( -5.354491962338109090, 6.146186931204312920, -0.06809871960538033120 ) ) ;
#8565=CARTESIAN_POINT ( 'NONE',  ( 8.000000000000007105, -4.618802153517121312, -0.7145311798163467287 ) ) ;
#8589=ORIENTED_EDGE ( 'NONE', *, *, #7620, .F. ) ;
#8590=AXIS2_PLACEMENT_3D ( 'NONE', #1462, #4119, #2811 ) ;
#8591=CARTESIAN_POINT ( 'NONE',  ( -7.999999999999998224, -1.555946510856077492, -0.06708870216334689163 ) ) ;
#8592=EDGE_LOOP ( 'NONE', ( #3772, #3796, #502, #4092, #3650, #2680 ) ) ;
#8597=ADVANCED_FACE ( 'NONE', ( #7953 ), #7835, .T. ) ;
#8600=ORIENTED_EDGE ( 'NONE', *, *, #87, .F. ) ;
#8664=COLOUR_RGB('Black',0.12,0.14,0.17);
#8665=FILL_AREA_STYLE_COLOUR('',#8664);
#8666=FILL_AREA_STYLE('',(#8665));
#8667=SURFACE_STYLE_FILL_AREA(#8666);
#8668=SURFACE_SIDE_STYLE('',(#8667));
#8669=SURFACE_STYLE_USAGE(.BOTH.,#8668);
#8670=PRESENTATION_STYLE_ASSIGNMENT((#8669));
ENDSEC;
END-ISO-10303-21;
